ISO-10303-21;
HEADER;
/* Generated by software containing ST-Developer
 * from STEP Tools, Inc. (www.steptools.com) 
 */

FILE_DESCRIPTION(
/* description */ ('Ball-type isolation valve (generic)'),
/* implementation_level */ '2;1');

FILE_NAME(
/* name */ 'Stop pin (1).step',
/* time_stamp */ '2026-10-27T10:53:05-07:00',
/* author */ (''),
/* organization */ (''),
/* preprocessor_version */ 'ST-DEVELOPER v20.2',
/* originating_system */ 'Autodesk Translation Framework v15.17.0.0',
/* authorisation */ '');

FILE_SCHEMA (('AUTOMOTIVE_DESIGN { 1 0 10303 214 3 1 1 }'));
ENDSEC;

DATA;
#10=MECHANICAL_DESIGN_GEOMETRIC_PRESENTATION_REPRESENTATION('',(#291),#7425);
#239=SHAPE_REPRESENTATION_RELATIONSHIP('SRR','None',#7549,#265);
#265=ADVANCED_BREP_SHAPE_REPRESENTATION('',(#317),#7412);
#291=STYLED_ITEM('',(#7744),#317);
#317=MANIFOLD_SOLID_BREP('Body1',#4096);
#480=PLANE('',#4641);
#481=PLANE('',#4642);
#694=FACE_OUTER_BOUND('',#1011,.T.);
#695=FACE_OUTER_BOUND('',#1012,.T.);
#696=FACE_OUTER_BOUND('',#1013,.T.);
#1011=EDGE_LOOP('',(#3231,#3232,#3233,#3234));
#1012=EDGE_LOOP('',(#3235));
#1013=EDGE_LOOP('',(#3236));
#1285=LINE('',#6717,#1593);
#1593=VECTOR('',#5500,0.3);
#1889=CIRCLE('',#4639,0.3);
#1890=CIRCLE('',#4640,0.3);
#2109=VERTEX_POINT('',#6714);
#2110=VERTEX_POINT('',#6716);
#2508=EDGE_CURVE('',#2109,#2109,#1889,.T.);
#2509=EDGE_CURVE('',#2109,#2110,#1285,.T.);
#2510=EDGE_CURVE('',#2110,#2110,#1890,.T.);
#3231=ORIENTED_EDGE('',*,*,#2508,.F.);
#3232=ORIENTED_EDGE('',*,*,#2509,.T.);
#3233=ORIENTED_EDGE('',*,*,#2510,.T.);
#3234=ORIENTED_EDGE('',*,*,#2509,.F.);
#3235=ORIENTED_EDGE('',*,*,#2508,.T.);
#3236=ORIENTED_EDGE('',*,*,#2510,.F.);
#3814=CYLINDRICAL_SURFACE('',#4638,0.3);
#3948=ADVANCED_FACE('',(#694),#3814,.T.);
#3949=ADVANCED_FACE('',(#695),#480,.T.);
#3950=ADVANCED_FACE('',(#696),#481,.F.);
#4096=CLOSED_SHELL('',(#3948,#3949,#3950));
#4637=AXIS2_PLACEMENT_3D('',#6712,#5494,#5495);
#4638=AXIS2_PLACEMENT_3D('',#6713,#5496,#5497);
#4639=AXIS2_PLACEMENT_3D('',#6715,#5498,#5499);
#4640=AXIS2_PLACEMENT_3D('',#6718,#5501,#5502);
#4641=AXIS2_PLACEMENT_3D('',#6719,#5503,#5504);
#4642=AXIS2_PLACEMENT_3D('',#6720,#5505,#5506);
#5494=DIRECTION('axis',(0.,0.,1.));
#5495=DIRECTION('refdir',(1.,0.,0.));
#5496=DIRECTION('center_axis',(0.,0.,1.));
#5497=DIRECTION('ref_axis',(1.,0.,0.));
#5498=DIRECTION('center_axis',(0.,0.,1.));
#5499=DIRECTION('ref_axis',(1.,0.,0.));
#5500=DIRECTION('',(0.,0.,-1.));
#5501=DIRECTION('center_axis',(0.,0.,1.));
#5502=DIRECTION('ref_axis',(1.,0.,0.));
#5503=DIRECTION('center_axis',(0.,0.,1.));
#5504=DIRECTION('ref_axis',(1.,0.,0.));
#5505=DIRECTION('center_axis',(0.,0.,1.));
#5506=DIRECTION('ref_axis',(1.,0.,0.));
#6712=CARTESIAN_POINT('',(0.,0.,0.));
#6713=CARTESIAN_POINT('Origin',(-1.1,-3.,8.2));
#6714=CARTESIAN_POINT('',(-1.4,-3.,9.4));
#6715=CARTESIAN_POINT('Origin',(-1.1,-3.,9.4));
#6716=CARTESIAN_POINT('',(-1.4,-3.,8.2));
#6717=CARTESIAN_POINT('',(-1.4,-3.,8.2));
#6718=CARTESIAN_POINT('Origin',(-1.1,-3.,8.2));
#6719=CARTESIAN_POINT('Origin',(-1.1,-3.,9.4));
#6720=CARTESIAN_POINT('Origin',(-1.1,-3.,8.2));
#7382=UNCERTAINTY_MEASURE_WITH_UNIT(LENGTH_MEASURE(0.001),#7426,
'DISTANCE_ACCURACY_VALUE',
'Maximum model space distance between geometric entities at asserted c
onnectivities');
#7395=UNCERTAINTY_MEASURE_WITH_UNIT(LENGTH_MEASURE(0.001),#7426,
'DISTANCE_ACCURACY_VALUE',
'Maximum model space distance between geometric entities at asserted c
onnectivities');
#7412=(
GEOMETRIC_REPRESENTATION_CONTEXT(3)
GLOBAL_UNCERTAINTY_ASSIGNED_CONTEXT((#7382))
GLOBAL_UNIT_ASSIGNED_CONTEXT((#7426,#7428,#7429))
REPRESENTATION_CONTEXT('','3D')
);
#7425=(
GEOMETRIC_REPRESENTATION_CONTEXT(3)
GLOBAL_UNCERTAINTY_ASSIGNED_CONTEXT((#7395))
GLOBAL_UNIT_ASSIGNED_CONTEXT((#7426,#7428,#7429))
REPRESENTATION_CONTEXT('','3D')
);
#7426=(
LENGTH_UNIT()
NAMED_UNIT(*)
SI_UNIT(.CENTI.,.METRE.)
);
#7428=(
NAMED_UNIT(*)
PLANE_ANGLE_UNIT()
SI_UNIT($,.RADIAN.)
);
#7429=(
NAMED_UNIT(*)
SI_UNIT($,.STERADIAN.)
SOLID_ANGLE_UNIT()
);
#7446=SHAPE_DEFINITION_REPRESENTATION(#7475,#7549);
#7475=PRODUCT_DEFINITION_SHAPE('',$,#7579);
#7549=SHAPE_REPRESENTATION('',(#4637),#7412);
#7562=PRODUCT_DEFINITION_CONTEXT('part definition',#7651,'design');
#7579=PRODUCT_DEFINITION('Stop pin (1)','Stop pin (1)',#7608,#7562);
#7608=PRODUCT_DEFINITION_FORMATION('',$,#7669);
#7651=APPLICATION_CONTEXT(
'Core Data for Automotive Mechanical Design Process');
#7652=PRODUCT_CONTEXT('part definition',#7651,'mechanical');
#7669=PRODUCT('Stop pin (1)','Stop pin (1)','Stop pin (1)',(#7652));
#7738=COLOUR_RGB('Grey',0.48,0.52,0.57);
#7739=FILL_AREA_STYLE_COLOUR('',#7738);
#7740=FILL_AREA_STYLE('',(#7739));
#7741=SURFACE_STYLE_FILL_AREA(#7740);
#7742=SURFACE_SIDE_STYLE('',(#7741));
#7743=SURFACE_STYLE_USAGE(.BOTH.,#7742);
#7744=PRESENTATION_STYLE_ASSIGNMENT((#7743));
ENDSEC;
END-ISO-10303-21;
